ISO-10303-21;
HEADER;
/* Generated by software containing ST-Developer
 * from STEP Tools, Inc. (www.steptools.com) 
 */

FILE_DESCRIPTION(
/* description */ (''),
/* implementation_level */ '2;1');

FILE_NAME(
/* name */ '10_Shaft_Key_5-32.step',
/* time_stamp */ '2026-10-26T06:59:52-07:00',
/* author */ (''),
/* organization */ (''),
/* preprocessor_version */ 'ST-DEVELOPER v20.2',
/* originating_system */ 'Autodesk Translation Framework v15.15.0.0',
/* authorisation */ '');

FILE_SCHEMA (('AUTOMOTIVE_DESIGN { 1 0 10303 214 3 1 1 }'));
ENDSEC;

DATA;
#10=MECHANICAL_DESIGN_GEOMETRIC_PRESENTATION_REPRESENTATION('',(#172),#46395);
#144=SHAPE_REPRESENTATION_RELATIONSHIP('SRR','None',#46464,#158);
#158=ADVANCED_BREP_SHAPE_REPRESENTATION('',(#186),#46389);
#172=STYLED_ITEM('',(#46596),#186);
#186=MANIFOLD_SOLID_BREP('Body1',#24945);
#1524=PLANE('',#26495);
#1525=PLANE('',#26496);
#1526=PLANE('',#26497);
#1527=PLANE('',#26498);
#1528=PLANE('',#26499);
#1529=PLANE('',#26500);
#1530=PLANE('',#26501);
#1531=PLANE('',#26502);
#1532=PLANE('',#26503);
#1533=PLANE('',#26504);
#1534=PLANE('',#26505);
#1535=PLANE('',#26506);
#1536=PLANE('',#26507);
#1537=PLANE('',#26508);
#1538=PLANE('',#26509);
#1539=PLANE('',#26510);
#1540=PLANE('',#26511);
#1541=PLANE('',#26512);
#2788=FACE_OUTER_BOUND('',#4198,.T.);
#2789=FACE_OUTER_BOUND('',#4199,.T.);
#2790=FACE_OUTER_BOUND('',#4200,.T.);
#2791=FACE_OUTER_BOUND('',#4201,.T.);
#2792=FACE_OUTER_BOUND('',#4202,.T.);
#2793=FACE_OUTER_BOUND('',#4203,.T.);
#2794=FACE_OUTER_BOUND('',#4204,.T.);
#2795=FACE_OUTER_BOUND('',#4205,.T.);
#2796=FACE_OUTER_BOUND('',#4206,.T.);
#2797=FACE_OUTER_BOUND('',#4207,.T.);
#2798=FACE_OUTER_BOUND('',#4208,.T.);
#2799=FACE_OUTER_BOUND('',#4209,.T.);
#2800=FACE_OUTER_BOUND('',#4210,.T.);
#2801=FACE_OUTER_BOUND('',#4211,.T.);
#2802=FACE_OUTER_BOUND('',#4212,.T.);
#2803=FACE_OUTER_BOUND('',#4213,.T.);
#2804=FACE_OUTER_BOUND('',#4214,.T.);
#2805=FACE_OUTER_BOUND('',#4215,.T.);
#4198=EDGE_LOOP('',(#22202,#22203,#22204,#22205,#22206,#22207));
#4199=EDGE_LOOP('',(#22208,#22209,#22210,#22211));
#4200=EDGE_LOOP('',(#22212,#22213,#22214,#22215,#22216,#22217));
#4201=EDGE_LOOP('',(#22218,#22219,#22220,#22221,#22222,#22223));
#4202=EDGE_LOOP('',(#22224,#22225,#22226,#22227,#22228,#22229));
#4203=EDGE_LOOP('',(#22230,#22231,#22232,#22233));
#4204=EDGE_LOOP('',(#22234,#22235,#22236,#22237,#22238,#22239));
#4205=EDGE_LOOP('',(#22240,#22241,#22242,#22243,#22244,#22245));
#4206=EDGE_LOOP('',(#22246,#22247,#22248,#22249));
#4207=EDGE_LOOP('',(#22250,#22251,#22252,#22253,#22254,#22255));
#4208=EDGE_LOOP('',(#22256,#22257,#22258,#22259,#22260,#22261));
#4209=EDGE_LOOP('',(#22262,#22263,#22264,#22265));
#4210=EDGE_LOOP('',(#22266,#22267,#22268,#22269,#22270,#22271));
#4211=EDGE_LOOP('',(#22272,#22273,#22274,#22275,#22276,#22277));
#4212=EDGE_LOOP('',(#22278,#22279,#22280,#22281,#22282,#22283));
#4213=EDGE_LOOP('',(#22284,#22285,#22286,#22287));
#4214=EDGE_LOOP('',(#22288,#22289,#22290,#22291,#22292,#22293));
#4215=EDGE_LOOP('',(#22294,#22295,#22296,#22297));
#6951=LINE('',#40344,#9820);
#6952=LINE('',#40346,#9821);
#6953=LINE('',#40348,#9822);
#6954=LINE('',#40350,#9823);
#6955=LINE('',#40352,#9824);
#6956=LINE('',#40353,#9825);
#6957=LINE('',#40356,#9826);
#6958=LINE('',#40358,#9827);
#6959=LINE('',#40359,#9828);
#6960=LINE('',#40362,#9829);
#6961=LINE('',#40364,#9830);
#6962=LINE('',#40366,#9831);
#6963=LINE('',#40367,#9832);
#6964=LINE('',#40370,#9833);
#6965=LINE('',#40372,#9834);
#6966=LINE('',#40374,#9835);
#6967=LINE('',#40375,#9836);
#6968=LINE('',#40378,#9837);
#6969=LINE('',#40380,#9838);
#6970=LINE('',#40382,#9839);
#6971=LINE('',#40384,#9840);
#6972=LINE('',#40385,#9841);
#6973=LINE('',#40388,#9842);
#6974=LINE('',#40390,#9843);
#6975=LINE('',#40391,#9844);
#6976=LINE('',#40394,#9845);
#6977=LINE('',#40396,#9846);
#6978=LINE('',#40398,#9847);
#6979=LINE('',#40399,#9848);
#6980=LINE('',#40402,#9849);
#6981=LINE('',#40403,#9850);
#6982=LINE('',#40404,#9851);
#6983=LINE('',#40407,#9852);
#6984=LINE('',#40408,#9853);
#6985=LINE('',#40411,#9854);
#6986=LINE('',#40413,#9855);
#6987=LINE('',#40415,#9856);
#6988=LINE('',#40416,#9857);
#6989=LINE('',#40419,#9858);
#6990=LINE('',#40420,#9859);
#6991=LINE('',#40421,#9860);
#6992=LINE('',#40424,#9861);
#6993=LINE('',#40425,#9862);
#6994=LINE('',#40428,#9863);
#6995=LINE('',#40430,#9864);
#6996=LINE('',#40431,#9865);
#6997=LINE('',#40433,#9866);
#6998=LINE('',#40435,#9867);
#9820=VECTOR('',#32130,10.);
#9821=VECTOR('',#32131,10.);
#9822=VECTOR('',#32132,10.);
#9823=VECTOR('',#32133,10.);
#9824=VECTOR('',#32134,10.);
#9825=VECTOR('',#32135,10.);
#9826=VECTOR('',#32138,10.);
#9827=VECTOR('',#32139,10.);
#9828=VECTOR('',#32140,10.);
#9829=VECTOR('',#32143,10.);
#9830=VECTOR('',#32144,10.);
#9831=VECTOR('',#32145,10.);
#9832=VECTOR('',#32146,10.);
#9833=VECTOR('',#32149,10.);
#9834=VECTOR('',#32150,10.);
#9835=VECTOR('',#32151,10.);
#9836=VECTOR('',#32152,10.);
#9837=VECTOR('',#32155,10.);
#9838=VECTOR('',#32156,10.);
#9839=VECTOR('',#32157,10.);
#9840=VECTOR('',#32158,10.);
#9841=VECTOR('',#32159,10.);
#9842=VECTOR('',#32162,10.);
#9843=VECTOR('',#32163,10.);
#9844=VECTOR('',#32164,10.);
#9845=VECTOR('',#32167,10.);
#9846=VECTOR('',#32168,10.);
#9847=VECTOR('',#32169,10.);
#9848=VECTOR('',#32170,10.);
#9849=VECTOR('',#32173,10.);
#9850=VECTOR('',#32174,10.);
#9851=VECTOR('',#32175,10.);
#9852=VECTOR('',#32178,10.);
#9853=VECTOR('',#32179,10.);
#9854=VECTOR('',#32182,10.);
#9855=VECTOR('',#32183,10.);
#9856=VECTOR('',#32184,10.);
#9857=VECTOR('',#32185,10.);
#9858=VECTOR('',#32188,10.);
#9859=VECTOR('',#32189,10.);
#9860=VECTOR('',#32190,10.);
#9861=VECTOR('',#32193,10.);
#9862=VECTOR('',#32194,10.);
#9863=VECTOR('',#32197,10.);
#9864=VECTOR('',#32198,10.);
#9865=VECTOR('',#32199,10.);
#9866=VECTOR('',#32202,10.);
#9867=VECTOR('',#32205,10.);
#12579=VERTEX_POINT('',#40342);
#12580=VERTEX_POINT('',#40343);
#12581=VERTEX_POINT('',#40345);
#12582=VERTEX_POINT('',#40347);
#12583=VERTEX_POINT('',#40349);
#12584=VERTEX_POINT('',#40351);
#12585=VERTEX_POINT('',#40355);
#12586=VERTEX_POINT('',#40357);
#12587=VERTEX_POINT('',#40361);
#12588=VERTEX_POINT('',#40363);
#12589=VERTEX_POINT('',#40365);
#12590=VERTEX_POINT('',#40369);
#12591=VERTEX_POINT('',#40371);
#12592=VERTEX_POINT('',#40373);
#12593=VERTEX_POINT('',#40377);
#12594=VERTEX_POINT('',#40379);
#12595=VERTEX_POINT('',#40381);
#12596=VERTEX_POINT('',#40383);
#12597=VERTEX_POINT('',#40387);
#12598=VERTEX_POINT('',#40389);
#12599=VERTEX_POINT('',#40393);
#12600=VERTEX_POINT('',#40395);
#12601=VERTEX_POINT('',#40397);
#12602=VERTEX_POINT('',#40401);
#12603=VERTEX_POINT('',#40406);
#12604=VERTEX_POINT('',#40410);
#12605=VERTEX_POINT('',#40412);
#12606=VERTEX_POINT('',#40414);
#12607=VERTEX_POINT('',#40418);
#12608=VERTEX_POINT('',#40423);
#12609=VERTEX_POINT('',#40427);
#12610=VERTEX_POINT('',#40429);
#15854=EDGE_CURVE('',#12579,#12580,#6951,.T.);
#15855=EDGE_CURVE('',#12580,#12581,#6952,.T.);
#15856=EDGE_CURVE('',#12581,#12582,#6953,.T.);
#15857=EDGE_CURVE('',#12582,#12583,#6954,.T.);
#15858=EDGE_CURVE('',#12583,#12584,#6955,.T.);
#15859=EDGE_CURVE('',#12584,#12579,#6956,.T.);
#15860=EDGE_CURVE('',#12585,#12583,#6957,.T.);
#15861=EDGE_CURVE('',#12586,#12585,#6958,.T.);
#15862=EDGE_CURVE('',#12584,#12586,#6959,.T.);
#15863=EDGE_CURVE('',#12587,#12582,#6960,.T.);
#15864=EDGE_CURVE('',#12587,#12588,#6961,.T.);
#15865=EDGE_CURVE('',#12589,#12588,#6962,.T.);
#15866=EDGE_CURVE('',#12585,#12589,#6963,.T.);
#15867=EDGE_CURVE('',#12581,#12590,#6964,.T.);
#15868=EDGE_CURVE('',#12591,#12590,#6965,.T.);
#15869=EDGE_CURVE('',#12591,#12592,#6966,.T.);
#15870=EDGE_CURVE('',#12592,#12587,#6967,.T.);
#15871=EDGE_CURVE('',#12590,#12593,#6968,.T.);
#15872=EDGE_CURVE('',#12593,#12594,#6969,.T.);
#15873=EDGE_CURVE('',#12594,#12595,#6970,.T.);
#15874=EDGE_CURVE('',#12595,#12596,#6971,.T.);
#15875=EDGE_CURVE('',#12596,#12591,#6972,.T.);
#15876=EDGE_CURVE('',#12597,#12595,#6973,.T.);
#15877=EDGE_CURVE('',#12598,#12597,#6974,.T.);
#15878=EDGE_CURVE('',#12596,#12598,#6975,.T.);
#15879=EDGE_CURVE('',#12599,#12594,#6976,.T.);
#15880=EDGE_CURVE('',#12599,#12600,#6977,.T.);
#15881=EDGE_CURVE('',#12601,#12600,#6978,.T.);
#15882=EDGE_CURVE('',#12597,#12601,#6979,.T.);
#15883=EDGE_CURVE('',#12579,#12602,#6980,.T.);
#15884=EDGE_CURVE('',#12602,#12599,#6981,.T.);
#15885=EDGE_CURVE('',#12593,#12580,#6982,.T.);
#15886=EDGE_CURVE('',#12603,#12592,#6983,.T.);
#15887=EDGE_CURVE('',#12588,#12603,#6984,.T.);
#15888=EDGE_CURVE('',#12601,#12604,#6985,.T.);
#15889=EDGE_CURVE('',#12604,#12605,#6986,.T.);
#15890=EDGE_CURVE('',#12605,#12606,#6987,.T.);
#15891=EDGE_CURVE('',#12606,#12598,#6988,.T.);
#15892=EDGE_CURVE('',#12605,#12607,#6989,.T.);
#15893=EDGE_CURVE('',#12607,#12589,#6990,.T.);
#15894=EDGE_CURVE('',#12603,#12606,#6991,.T.);
#15895=EDGE_CURVE('',#12608,#12604,#6992,.T.);
#15896=EDGE_CURVE('',#12607,#12608,#6993,.T.);
#15897=EDGE_CURVE('',#12600,#12609,#6994,.T.);
#15898=EDGE_CURVE('',#12609,#12610,#6995,.T.);
#15899=EDGE_CURVE('',#12608,#12610,#6996,.T.);
#15900=EDGE_CURVE('',#12610,#12586,#6997,.T.);
#15901=EDGE_CURVE('',#12609,#12602,#6998,.T.);
#22202=ORIENTED_EDGE('',*,*,#15854,.T.);
#22203=ORIENTED_EDGE('',*,*,#15855,.T.);
#22204=ORIENTED_EDGE('',*,*,#15856,.T.);
#22205=ORIENTED_EDGE('',*,*,#15857,.T.);
#22206=ORIENTED_EDGE('',*,*,#15858,.T.);
#22207=ORIENTED_EDGE('',*,*,#15859,.T.);
#22208=ORIENTED_EDGE('',*,*,#15858,.F.);
#22209=ORIENTED_EDGE('',*,*,#15860,.F.);
#22210=ORIENTED_EDGE('',*,*,#15861,.F.);
#22211=ORIENTED_EDGE('',*,*,#15862,.F.);
#22212=ORIENTED_EDGE('',*,*,#15857,.F.);
#22213=ORIENTED_EDGE('',*,*,#15863,.F.);
#22214=ORIENTED_EDGE('',*,*,#15864,.T.);
#22215=ORIENTED_EDGE('',*,*,#15865,.F.);
#22216=ORIENTED_EDGE('',*,*,#15866,.F.);
#22217=ORIENTED_EDGE('',*,*,#15860,.T.);
#22218=ORIENTED_EDGE('',*,*,#15856,.F.);
#22219=ORIENTED_EDGE('',*,*,#15867,.T.);
#22220=ORIENTED_EDGE('',*,*,#15868,.F.);
#22221=ORIENTED_EDGE('',*,*,#15869,.T.);
#22222=ORIENTED_EDGE('',*,*,#15870,.T.);
#22223=ORIENTED_EDGE('',*,*,#15863,.T.);
#22224=ORIENTED_EDGE('',*,*,#15868,.T.);
#22225=ORIENTED_EDGE('',*,*,#15871,.T.);
#22226=ORIENTED_EDGE('',*,*,#15872,.T.);
#22227=ORIENTED_EDGE('',*,*,#15873,.T.);
#22228=ORIENTED_EDGE('',*,*,#15874,.T.);
#22229=ORIENTED_EDGE('',*,*,#15875,.T.);
#22230=ORIENTED_EDGE('',*,*,#15874,.F.);
#22231=ORIENTED_EDGE('',*,*,#15876,.F.);
#22232=ORIENTED_EDGE('',*,*,#15877,.F.);
#22233=ORIENTED_EDGE('',*,*,#15878,.F.);
#22234=ORIENTED_EDGE('',*,*,#15873,.F.);
#22235=ORIENTED_EDGE('',*,*,#15879,.F.);
#22236=ORIENTED_EDGE('',*,*,#15880,.T.);
#22237=ORIENTED_EDGE('',*,*,#15881,.F.);
#22238=ORIENTED_EDGE('',*,*,#15882,.F.);
#22239=ORIENTED_EDGE('',*,*,#15876,.T.);
#22240=ORIENTED_EDGE('',*,*,#15854,.F.);
#22241=ORIENTED_EDGE('',*,*,#15883,.T.);
#22242=ORIENTED_EDGE('',*,*,#15884,.T.);
#22243=ORIENTED_EDGE('',*,*,#15879,.T.);
#22244=ORIENTED_EDGE('',*,*,#15872,.F.);
#22245=ORIENTED_EDGE('',*,*,#15885,.T.);
#22246=ORIENTED_EDGE('',*,*,#15870,.F.);
#22247=ORIENTED_EDGE('',*,*,#15886,.F.);
#22248=ORIENTED_EDGE('',*,*,#15887,.F.);
#22249=ORIENTED_EDGE('',*,*,#15864,.F.);
#22250=ORIENTED_EDGE('',*,*,#15888,.T.);
#22251=ORIENTED_EDGE('',*,*,#15889,.T.);
#22252=ORIENTED_EDGE('',*,*,#15890,.T.);
#22253=ORIENTED_EDGE('',*,*,#15891,.T.);
#22254=ORIENTED_EDGE('',*,*,#15877,.T.);
#22255=ORIENTED_EDGE('',*,*,#15882,.T.);
#22256=ORIENTED_EDGE('',*,*,#15890,.F.);
#22257=ORIENTED_EDGE('',*,*,#15892,.T.);
#22258=ORIENTED_EDGE('',*,*,#15893,.T.);
#22259=ORIENTED_EDGE('',*,*,#15865,.T.);
#22260=ORIENTED_EDGE('',*,*,#15887,.T.);
#22261=ORIENTED_EDGE('',*,*,#15894,.T.);
#22262=ORIENTED_EDGE('',*,*,#15889,.F.);
#22263=ORIENTED_EDGE('',*,*,#15895,.F.);
#22264=ORIENTED_EDGE('',*,*,#15896,.F.);
#22265=ORIENTED_EDGE('',*,*,#15892,.F.);
#22266=ORIENTED_EDGE('',*,*,#15888,.F.);
#22267=ORIENTED_EDGE('',*,*,#15881,.T.);
#22268=ORIENTED_EDGE('',*,*,#15897,.T.);
#22269=ORIENTED_EDGE('',*,*,#15898,.T.);
#22270=ORIENTED_EDGE('',*,*,#15899,.F.);
#22271=ORIENTED_EDGE('',*,*,#15895,.T.);
#22272=ORIENTED_EDGE('',*,*,#15893,.F.);
#22273=ORIENTED_EDGE('',*,*,#15896,.T.);
#22274=ORIENTED_EDGE('',*,*,#15899,.T.);
#22275=ORIENTED_EDGE('',*,*,#15900,.T.);
#22276=ORIENTED_EDGE('',*,*,#15861,.T.);
#22277=ORIENTED_EDGE('',*,*,#15866,.T.);
#22278=ORIENTED_EDGE('',*,*,#15859,.F.);
#22279=ORIENTED_EDGE('',*,*,#15862,.T.);
#22280=ORIENTED_EDGE('',*,*,#15900,.F.);
#22281=ORIENTED_EDGE('',*,*,#15898,.F.);
#22282=ORIENTED_EDGE('',*,*,#15901,.T.);
#22283=ORIENTED_EDGE('',*,*,#15883,.F.);
#22284=ORIENTED_EDGE('',*,*,#15884,.F.);
#22285=ORIENTED_EDGE('',*,*,#15901,.F.);
#22286=ORIENTED_EDGE('',*,*,#15897,.F.);
#22287=ORIENTED_EDGE('',*,*,#15880,.F.);
#22288=ORIENTED_EDGE('',*,*,#15875,.F.);
#22289=ORIENTED_EDGE('',*,*,#15878,.T.);
#22290=ORIENTED_EDGE('',*,*,#15891,.F.);
#22291=ORIENTED_EDGE('',*,*,#15894,.F.);
#22292=ORIENTED_EDGE('',*,*,#15886,.T.);
#22293=ORIENTED_EDGE('',*,*,#15869,.F.);
#22294=ORIENTED_EDGE('',*,*,#15855,.F.);
#22295=ORIENTED_EDGE('',*,*,#15885,.F.);
#22296=ORIENTED_EDGE('',*,*,#15871,.F.);
#22297=ORIENTED_EDGE('',*,*,#15867,.F.);
#24647=ADVANCED_FACE('',(#2788),#1524,.T.);
#24648=ADVANCED_FACE('',(#2789),#1525,.T.);
#24649=ADVANCED_FACE('',(#2790),#1526,.T.);
#24650=ADVANCED_FACE('',(#2791),#1527,.T.);
#24651=ADVANCED_FACE('',(#2792),#1528,.T.);
#24652=ADVANCED_FACE('',(#2793),#1529,.T.);
#24653=ADVANCED_FACE('',(#2794),#1530,.T.);
#24654=ADVANCED_FACE('',(#2795),#1531,.T.);
#24655=ADVANCED_FACE('',(#2796),#1532,.T.);
#24656=ADVANCED_FACE('',(#2797),#1533,.T.);
#24657=ADVANCED_FACE('',(#2798),#1534,.T.);
#24658=ADVANCED_FACE('',(#2799),#1535,.T.);
#24659=ADVANCED_FACE('',(#2800),#1536,.T.);
#24660=ADVANCED_FACE('',(#2801),#1537,.T.);
#24661=ADVANCED_FACE('',(#2802),#1538,.T.);
#24662=ADVANCED_FACE('',(#2803),#1539,.T.);
#24663=ADVANCED_FACE('',(#2804),#1540,.T.);
#24664=ADVANCED_FACE('',(#2805),#1541,.F.);
#24945=CLOSED_SHELL('',(#24647,#24648,#24649,#24650,#24651,#24652,#24653,
#24654,#24655,#24656,#24657,#24658,#24659,#24660,#24661,#24662,#24663,#24664));
#26494=AXIS2_PLACEMENT_3D('',#40340,#32126,#32127);
#26495=AXIS2_PLACEMENT_3D('',#40341,#32128,#32129);
#26496=AXIS2_PLACEMENT_3D('',#40354,#32136,#32137);
#26497=AXIS2_PLACEMENT_3D('',#40360,#32141,#32142);
#26498=AXIS2_PLACEMENT_3D('',#40368,#32147,#32148);
#26499=AXIS2_PLACEMENT_3D('',#40376,#32153,#32154);
#26500=AXIS2_PLACEMENT_3D('',#40386,#32160,#32161);
#26501=AXIS2_PLACEMENT_3D('',#40392,#32165,#32166);
#26502=AXIS2_PLACEMENT_3D('',#40400,#32171,#32172);
#26503=AXIS2_PLACEMENT_3D('',#40405,#32176,#32177);
#26504=AXIS2_PLACEMENT_3D('',#40409,#32180,#32181);
#26505=AXIS2_PLACEMENT_3D('',#40417,#32186,#32187);
#26506=AXIS2_PLACEMENT_3D('',#40422,#32191,#32192);
#26507=AXIS2_PLACEMENT_3D('',#40426,#32195,#32196);
#26508=AXIS2_PLACEMENT_3D('',#40432,#32200,#32201);
#26509=AXIS2_PLACEMENT_3D('',#40434,#32203,#32204);
#26510=AXIS2_PLACEMENT_3D('',#40436,#32206,#32207);
#26511=AXIS2_PLACEMENT_3D('',#40437,#32208,#32209);
#26512=AXIS2_PLACEMENT_3D('',#40438,#32210,#32211);
#32126=DIRECTION('axis',(0.,0.,1.));
#32127=DIRECTION('refdir',(1.,0.,0.));
#32128=DIRECTION('center_axis',(0.707106781186548,-0.707106781186548,0.));
#32129=DIRECTION('ref_axis',(0.,0.,-1.));
#32130=DIRECTION('',(-0.577350269189626,-0.577350269189626,-0.577350269189626));
#32131=DIRECTION('',(0.,0.,-1.));
#32132=DIRECTION('',(0.577350269189626,0.577350269189626,-0.577350269189626));
#32133=DIRECTION('',(0.577350269189626,0.577350269189626,0.577350269189626));
#32134=DIRECTION('',(0.,0.,1.));
#32135=DIRECTION('',(-0.577350269189627,-0.577350269189627,0.577350269189624));
#32136=DIRECTION('center_axis',(1.,0.,0.));
#32137=DIRECTION('ref_axis',(0.,0.,-1.));
#32138=DIRECTION('',(0.,-1.,0.));
#32139=DIRECTION('',(0.,0.,-1.));
#32140=DIRECTION('',(0.,1.,0.));
#32141=DIRECTION('center_axis',(0.707106781186548,0.,-0.707106781186548));
#32142=DIRECTION('ref_axis',(-0.707106781186548,0.,-0.707106781186548));
#32143=DIRECTION('',(0.577350269189626,-0.577350269189626,0.577350269189626));
#32144=DIRECTION('',(0.,1.,0.));
#32145=DIRECTION('',(-0.577350269189624,-0.57735026918963,-0.577350269189624));
#32146=DIRECTION('',(-0.577350269189624,0.57735026918963,-0.577350269189624));
#32147=DIRECTION('center_axis',(0.,-0.707106781186548,-0.707106781186548));
#32148=DIRECTION('ref_axis',(-1.,0.,0.));
#32149=DIRECTION('',(-1.,0.,0.));
#32150=DIRECTION('',(0.577350269189626,-0.577350269189626,0.577350269189626));
#32151=DIRECTION('',(0.577350269189628,0.577350269189625,-0.577350269189625));
#32152=DIRECTION('',(1.,0.,0.));
#32153=DIRECTION('center_axis',(-0.707106781186548,-0.707106781186548,0.));
#32154=DIRECTION('ref_axis',(0.,0.,1.));
#32155=DIRECTION('',(0.,0.,1.));
#32156=DIRECTION('',(-0.577350269189626,0.577350269189626,0.577350269189626));
#32157=DIRECTION('',(-0.577350269189626,0.577350269189626,-0.577350269189626));
#32158=DIRECTION('',(0.,0.,-1.));
#32159=DIRECTION('',(0.577350269189627,-0.577350269189627,-0.577350269189624));
#32160=DIRECTION('center_axis',(-1.,0.,0.));
#32161=DIRECTION('ref_axis',(0.,0.,1.));
#32162=DIRECTION('',(0.,-1.,0.));
#32163=DIRECTION('',(0.,0.,1.));
#32164=DIRECTION('',(0.,1.,0.));
#32165=DIRECTION('center_axis',(-0.707106781186548,0.,0.707106781186548));
#32166=DIRECTION('ref_axis',(0.707106781186548,0.,0.707106781186548));
#32167=DIRECTION('',(-0.577350269189626,-0.577350269189626,-0.577350269189626));
#32168=DIRECTION('',(0.,1.,0.));
#32169=DIRECTION('',(0.577350269189624,-0.57735026918963,0.577350269189624));
#32170=DIRECTION('',(0.577350269189624,0.57735026918963,0.577350269189624));
#32171=DIRECTION('center_axis',(0.,-0.707106781186548,0.707106781186548));
#32172=DIRECTION('ref_axis',(1.,0.,0.));
#32173=DIRECTION('',(-0.577350269189628,0.577350269189625,0.577350269189625));
#32174=DIRECTION('',(-1.,0.,0.));
#32175=DIRECTION('',(1.,0.,0.));
#32176=DIRECTION('center_axis',(0.,0.,-1.));
#32177=DIRECTION('ref_axis',(-1.,0.,0.));
#32178=DIRECTION('',(0.,-1.,0.));
#32179=DIRECTION('',(-1.,0.,0.));
#32180=DIRECTION('center_axis',(-0.707106781186551,0.707106781186544,0.));
#32181=DIRECTION('ref_axis',(0.,0.,1.));
#32182=DIRECTION('',(0.577350269189624,0.57735026918963,-0.577350269189624));
#32183=DIRECTION('',(0.,0.,-1.));
#32184=DIRECTION('',(-0.577350269189624,-0.57735026918963,-0.577350269189624));
#32185=DIRECTION('',(-0.577350269189625,-0.577350269189631,0.577350269189622));
#32186=DIRECTION('center_axis',(0.,0.707106781186544,-0.707106781186551));
#32187=DIRECTION('ref_axis',(-1.,0.,0.));
#32188=DIRECTION('',(1.,0.,0.));
#32189=DIRECTION('',(0.577350269189624,-0.57735026918963,-0.577350269189624));
#32190=DIRECTION('',(-0.577350269189625,0.577350269189629,0.577350269189623));
#32191=DIRECTION('center_axis',(0.,1.,0.));
#32192=DIRECTION('ref_axis',(0.,0.,1.));
#32193=DIRECTION('',(-1.,0.,0.));
#32194=DIRECTION('',(0.,0.,1.));
#32195=DIRECTION('center_axis',(0.,0.707106781186544,0.707106781186551));
#32196=DIRECTION('ref_axis',(1.,0.,0.));
#32197=DIRECTION('',(1.,0.,0.));
#32198=DIRECTION('',(0.577350269189625,0.577350269189629,-0.577350269189623));
#32199=DIRECTION('',(0.577350269189624,-0.57735026918963,0.577350269189624));
#32200=DIRECTION('center_axis',(0.707106781186551,0.707106781186544,0.));
#32201=DIRECTION('ref_axis',(0.,0.,-1.));
#32202=DIRECTION('',(0.577350269189625,-0.577350269189631,-0.577350269189622));
#32203=DIRECTION('center_axis',(0.707106781186546,0.,0.707106781186549));
#32204=DIRECTION('ref_axis',(0.707106781186549,0.,-0.707106781186546));
#32205=DIRECTION('',(0.,-1.,0.));
#32206=DIRECTION('center_axis',(0.,0.,1.));
#32207=DIRECTION('ref_axis',(1.,0.,0.));
#32208=DIRECTION('center_axis',(-0.707106781186546,0.,-0.707106781186549));
#32209=DIRECTION('ref_axis',(-0.707106781186549,0.,0.707106781186546));
#32210=DIRECTION('center_axis',(0.,1.,0.));
#32211=DIRECTION('ref_axis',(1.,0.,0.));
#40340=CARTESIAN_POINT('',(0.,0.,0.));
#40341=CARTESIAN_POINT('Origin',(1.885,-34.8,8.9275));
#40342=CARTESIAN_POINT('',(1.86,-34.825,9.795));
#40343=CARTESIAN_POINT('',(1.785,-34.9,9.72));
#40344=CARTESIAN_POINT('',(1.25666666666667,-35.4283333333333,9.19166666666666));
#40345=CARTESIAN_POINT('',(1.785,-34.9,6.15));
#40346=CARTESIAN_POINT('',(1.785,-34.9,8.9275));
#40347=CARTESIAN_POINT('',(1.86,-34.825,6.075));
#40348=CARTESIAN_POINT('',(1.25666666666667,-35.4283333333333,6.67833333333333));
#40349=CARTESIAN_POINT('',(1.985,-34.7,6.2));
#40350=CARTESIAN_POINT('',(2.33125,-34.35375,6.54625));
#40351=CARTESIAN_POINT('',(1.985,-34.7,9.67));
#40352=CARTESIAN_POINT('',(1.985,-34.7,8.9275));
#40353=CARTESIAN_POINT('',(2.00041666666667,-34.6845833333333,9.65458333333333));
#40354=CARTESIAN_POINT('Origin',(1.985,-34.9,9.92));
#40355=CARTESIAN_POINT('',(1.985,-10.3,6.2));
#40356=CARTESIAN_POINT('',(1.985,-34.9,6.2));
#40357=CARTESIAN_POINT('',(1.985,-10.3,9.67));
#40358=CARTESIAN_POINT('',(1.985,-10.3,8.9275));
#40359=CARTESIAN_POINT('',(1.985,-34.9,9.67));
#40360=CARTESIAN_POINT('Origin',(1.86,-34.9,6.075));
#40361=CARTESIAN_POINT('',(1.735,-34.7,5.95));
#40362=CARTESIAN_POINT('',(1.71958333333333,-34.6845833333333,5.93458333333333));
#40363=CARTESIAN_POINT('',(1.735,-10.3,5.95));
#40364=CARTESIAN_POINT('',(1.735,-34.9,5.95));
#40365=CARTESIAN_POINT('',(1.86,-10.175,6.075));
#40366=CARTESIAN_POINT('',(-2.41375000000001,-14.4487500000001,1.80124999999999));
#40367=CARTESIAN_POINT('',(6.46458333333334,-14.7795833333334,10.6795833333333));
#40368=CARTESIAN_POINT('Origin',(0.9925,-34.8,6.05));
#40369=CARTESIAN_POINT('',(-1.785,-34.9,6.15));
#40370=CARTESIAN_POINT('',(0.9925,-34.9,6.15));
#40371=CARTESIAN_POINT('',(-1.86,-34.825,6.075));
#40372=CARTESIAN_POINT('',(-1.25666666666667,-35.4283333333333,6.67833333333333));
#40373=CARTESIAN_POINT('',(-1.735,-34.7,5.95));
#40374=CARTESIAN_POINT('',(-1.38875,-34.35375,5.60375));
#40375=CARTESIAN_POINT('',(0.9925,-34.7,5.95));
#40376=CARTESIAN_POINT('Origin',(-1.885,-34.8,6.9425));
#40377=CARTESIAN_POINT('',(-1.785,-34.9,9.72));
#40378=CARTESIAN_POINT('',(-1.785,-34.9,6.9425));
#40379=CARTESIAN_POINT('',(-1.86,-34.825,9.795));
#40380=CARTESIAN_POINT('',(-1.25666666666667,-35.4283333333333,9.19166666666667));
#40381=CARTESIAN_POINT('',(-1.985,-34.7,9.67));
#40382=CARTESIAN_POINT('',(-2.33125,-34.35375,9.32375));
#40383=CARTESIAN_POINT('',(-1.985,-34.7,6.2));
#40384=CARTESIAN_POINT('',(-1.985,-34.7,6.9425));
#40385=CARTESIAN_POINT('',(-2.00041666666667,-34.6845833333333,6.21541666666666));
#40386=CARTESIAN_POINT('Origin',(-1.985,-34.9,5.95));
#40387=CARTESIAN_POINT('',(-1.985,-10.3,9.67));
#40388=CARTESIAN_POINT('',(-1.985,-34.9,9.67));
#40389=CARTESIAN_POINT('',(-1.985,-10.3,6.2));
#40390=CARTESIAN_POINT('',(-1.985,-10.3,6.9425));
#40391=CARTESIAN_POINT('',(-1.985,-34.9,6.2));
#40392=CARTESIAN_POINT('Origin',(-1.86,-34.9,9.795));
#40393=CARTESIAN_POINT('',(-1.735,-34.7,9.92));
#40394=CARTESIAN_POINT('',(-1.71958333333333,-34.6845833333333,9.93541666666667));
#40395=CARTESIAN_POINT('',(-1.735,-10.3,9.92));
#40396=CARTESIAN_POINT('',(-1.735,-34.9,9.92));
#40397=CARTESIAN_POINT('',(-1.86,-10.175,9.795));
#40398=CARTESIAN_POINT('',(2.41375000000001,-14.4487500000001,14.06875));
#40399=CARTESIAN_POINT('',(-6.46458333333334,-14.7795833333334,5.19041666666666));
#40400=CARTESIAN_POINT('Origin',(-0.9925,-34.8,9.82));
#40401=CARTESIAN_POINT('',(1.735,-34.7,9.92));
#40402=CARTESIAN_POINT('',(1.38875,-34.35375,10.26625));
#40403=CARTESIAN_POINT('',(-0.9925,-34.7,9.92));
#40404=CARTESIAN_POINT('',(-0.9925,-34.9,9.72));
#40405=CARTESIAN_POINT('Origin',(1.985,-34.9,5.95));
#40406=CARTESIAN_POINT('',(-1.735,-10.3,5.95));
#40407=CARTESIAN_POINT('',(-1.735,-34.9,5.95));
#40408=CARTESIAN_POINT('',(0.9925,-10.3,5.95));
#40409=CARTESIAN_POINT('Origin',(-1.885,-10.2,6.9425));
#40410=CARTESIAN_POINT('',(-1.785,-10.1,9.72));
#40411=CARTESIAN_POINT('',(-1.25666666666667,-9.57166666666666,9.19166666666667));
#40412=CARTESIAN_POINT('',(-1.785,-10.1,6.15));
#40413=CARTESIAN_POINT('',(-1.785,-10.1,6.9425));
#40414=CARTESIAN_POINT('',(-1.86,-10.175,6.075));
#40415=CARTESIAN_POINT('',(-1.25666666666667,-9.57166666666666,6.67833333333333));
#40416=CARTESIAN_POINT('',(-6.13375000000003,-14.4487500000001,10.34875));
#40417=CARTESIAN_POINT('Origin',(0.9925,-10.2,6.05));
#40418=CARTESIAN_POINT('',(1.785,-10.1,6.15));
#40419=CARTESIAN_POINT('',(0.9925,-10.1,6.15));
#40420=CARTESIAN_POINT('',(1.25666666666667,-9.57166666666666,6.67833333333333));
#40421=CARTESIAN_POINT('',(2.74458333333335,-14.7795833333334,1.47041666666667));
#40422=CARTESIAN_POINT('Origin',(0.,-10.1,7.935));
#40423=CARTESIAN_POINT('',(1.785,-10.1,9.72));
#40424=CARTESIAN_POINT('',(-0.9925,-10.1,9.72));
#40425=CARTESIAN_POINT('',(1.785,-10.1,8.9275));
#40426=CARTESIAN_POINT('Origin',(-0.9925,-10.2,9.82));
#40427=CARTESIAN_POINT('',(1.735,-10.3,9.92));
#40428=CARTESIAN_POINT('',(-0.9925,-10.3,9.92));
#40429=CARTESIAN_POINT('',(1.86,-10.175,9.795));
#40430=CARTESIAN_POINT('',(-2.74458333333335,-14.7795833333334,14.3995833333333));
#40431=CARTESIAN_POINT('',(1.25666666666667,-9.57166666666666,9.19166666666667));
#40432=CARTESIAN_POINT('Origin',(1.885,-10.2,8.9275));
#40433=CARTESIAN_POINT('',(6.13375000000003,-14.4487500000001,5.52124999999999));
#40434=CARTESIAN_POINT('Origin',(1.86,-34.9,9.795));
#40435=CARTESIAN_POINT('',(1.735,-34.9,9.92));
#40436=CARTESIAN_POINT('Origin',(-1.985,-34.9,9.92));
#40437=CARTESIAN_POINT('Origin',(-1.86,-34.9,6.075));
#40438=CARTESIAN_POINT('Origin',(0.,-34.9,7.935));
#46373=UNCERTAINTY_MEASURE_WITH_UNIT(LENGTH_MEASURE(0.01),#46396,
'DISTANCE_ACCURACY_VALUE',
'Maximum model space distance between geometric entities at asserted c
onnectivities');
#46379=UNCERTAINTY_MEASURE_WITH_UNIT(LENGTH_MEASURE(0.01),#46396,
'DISTANCE_ACCURACY_VALUE',
'Maximum model space distance between geometric entities at asserted c
onnectivities');
#46389=(
GEOMETRIC_REPRESENTATION_CONTEXT(3)
GLOBAL_UNCERTAINTY_ASSIGNED_CONTEXT((#46373))
GLOBAL_UNIT_ASSIGNED_CONTEXT((#46396,#46398,#46399))
REPRESENTATION_CONTEXT('','3D')
);
#46395=(
GEOMETRIC_REPRESENTATION_CONTEXT(3)
GLOBAL_UNCERTAINTY_ASSIGNED_CONTEXT((#46379))
GLOBAL_UNIT_ASSIGNED_CONTEXT((#46396,#46398,#46399))
REPRESENTATION_CONTEXT('','3D')
);
#46396=(
LENGTH_UNIT()
NAMED_UNIT(*)
SI_UNIT(.MILLI.,.METRE.)
);
#46398=(
NAMED_UNIT(*)
PLANE_ANGLE_UNIT()
SI_UNIT($,.RADIAN.)
);
#46399=(
NAMED_UNIT(*)
SI_UNIT($,.STERADIAN.)
SOLID_ANGLE_UNIT()
);
#46409=SHAPE_DEFINITION_REPRESENTATION(#46424,#46464);
#46424=PRODUCT_DEFINITION_SHAPE('',$,#46480);
#46464=SHAPE_REPRESENTATION('',(#26494),#46389);
#46470=PRODUCT_DEFINITION_CONTEXT('part definition',#46517,'design');
#46480=PRODUCT_DEFINITION('2026-10-26-00-51-14-660','10_Shaft_Key_5-32',
#46495,#46470);
#46495=PRODUCT_DEFINITION_FORMATION('',$,#46528);
#46517=APPLICATION_CONTEXT(
'Core Data for Automotive Mechanical Design Process');
#46518=PRODUCT_CONTEXT('part definition',#46517,'mechanical');
#46528=PRODUCT('2026-10-26-00-51-14-660','10_Shaft_Key_5-32',$,(#46518));
#46590=COLOUR_RGB('Grey',0.48,0.52,0.57);
#46591=FILL_AREA_STYLE_COLOUR('',#46590);
#46592=FILL_AREA_STYLE('',(#46591));
#46593=SURFACE_STYLE_FILL_AREA(#46592);
#46594=SURFACE_SIDE_STYLE('',(#46593));
#46595=SURFACE_STYLE_USAGE(.BOTH.,#46594);
#46596=PRESENTATION_STYLE_ASSIGNMENT((#46595));
ENDSEC;
END-ISO-10303-21;
